ISO-10303-21;
HEADER;
/* Generated by software containing ST-Developer
 * from STEP Tools, Inc. (www.steptools.com) 
 */

FILE_DESCRIPTION(
/* description */ ('STEP AP214'),
/* implementation_level */ '2;1');

FILE_NAME(
/* name */ 'Ball Screw Spacer 1.step',
/* time_stamp */ '2026-11-15T14:55:55-08:00',
/* author */ (''),
/* organization */ (''),
/* preprocessor_version */ 'ST-DEVELOPER v20.2',
/* originating_system */ 'Autodesk Translation Framework v15.17.0.0',
/* authorisation */ '');

FILE_SCHEMA (('AUTOMOTIVE_DESIGN { 1 0 10303 214 3 1 1 }'));
ENDSEC;

DATA;
#10=MECHANICAL_DESIGN_GEOMETRIC_PRESENTATION_REPRESENTATION('',(#936),#57079);
#876=SHAPE_REPRESENTATION_RELATIONSHIP('SRR','None',#57262,#905);
#905=ADVANCED_BREP_SHAPE_REPRESENTATION('',(#973),#57054);
#936=STYLED_ITEM('',(#57444),#973);
#973=MANIFOLD_SOLID_BREP('Body1',#24536);
#1093=FACE_BOUND('',#3901,.T.);
#1094=FACE_BOUND('',#3902,.T.);
#1095=FACE_BOUND('',#3903,.T.);
#1096=FACE_BOUND('',#3904,.T.);
#1097=FACE_BOUND('',#3910,.T.);
#1098=FACE_BOUND('',#3911,.T.);
#1099=FACE_BOUND('',#3912,.T.);
#1100=FACE_BOUND('',#3913,.T.);
#1500=PLANE('',#25385);
#1501=PLANE('',#25386);
#1502=PLANE('',#25387);
#1503=PLANE('',#25388);
#1504=PLANE('',#25389);
#1505=PLANE('',#25390);
#1506=PLANE('',#25391);
#1507=PLANE('',#25392);
#1508=PLANE('',#25393);
#1509=PLANE('',#25394);
#1510=PLANE('',#25395);
#1511=PLANE('',#25396);
#2422=FACE_OUTER_BOUND('',#3890,.T.);
#2423=FACE_OUTER_BOUND('',#3891,.T.);
#2424=FACE_OUTER_BOUND('',#3892,.T.);
#2425=FACE_OUTER_BOUND('',#3893,.T.);
#2426=FACE_OUTER_BOUND('',#3894,.T.);
#2427=FACE_OUTER_BOUND('',#3895,.T.);
#2428=FACE_OUTER_BOUND('',#3896,.T.);
#2429=FACE_OUTER_BOUND('',#3897,.T.);
#2430=FACE_OUTER_BOUND('',#3898,.T.);
#2431=FACE_OUTER_BOUND('',#3899,.T.);
#2432=FACE_OUTER_BOUND('',#3900,.T.);
#2433=FACE_OUTER_BOUND('',#3905,.T.);
#2434=FACE_OUTER_BOUND('',#3906,.T.);
#2435=FACE_OUTER_BOUND('',#3907,.T.);
#2436=FACE_OUTER_BOUND('',#3908,.T.);
#2437=FACE_OUTER_BOUND('',#3909,.T.);
#3890=EDGE_LOOP('',(#17096,#17097,#17098,#17099));
#3891=EDGE_LOOP('',(#17100,#17101,#17102,#17103));
#3892=EDGE_LOOP('',(#17104,#17105,#17106,#17107));
#3893=EDGE_LOOP('',(#17108,#17109,#17110,#17111));
#3894=EDGE_LOOP('',(#17112,#17113,#17114,#17115));
#3895=EDGE_LOOP('',(#17116,#17117,#17118,#17119,#17120,#17121));
#3896=EDGE_LOOP('',(#17122,#17123,#17124,#17125,#17126,#17127));
#3897=EDGE_LOOP('',(#17128,#17129,#17130,#17131,#17132,#17133));
#3898=EDGE_LOOP('',(#17134,#17135,#17136,#17137,#17138,#17139));
#3899=EDGE_LOOP('',(#17140,#17141,#17142,#17143));
#3900=EDGE_LOOP('',(#17144,#17145,#17146,#17147));
#3901=EDGE_LOOP('',(#17148));
#3902=EDGE_LOOP('',(#17149));
#3903=EDGE_LOOP('',(#17150));
#3904=EDGE_LOOP('',(#17151));
#3905=EDGE_LOOP('',(#17152,#17153,#17154,#17155));
#3906=EDGE_LOOP('',(#17156,#17157,#17158,#17159));
#3907=EDGE_LOOP('',(#17160,#17161,#17162,#17163));
#3908=EDGE_LOOP('',(#17164,#17165,#17166,#17167));
#3909=EDGE_LOOP('',(#17168,#17169,#17170,#17171,#17172,#17173,#17174,#17175));
#3910=EDGE_LOOP('',(#17176));
#3911=EDGE_LOOP('',(#17177));
#3912=EDGE_LOOP('',(#17178));
#3913=EDGE_LOOP('',(#17179));
#5621=LINE('',#36122,#7588);
#5622=LINE('',#36128,#7589);
#5623=LINE('',#36134,#7590);
#5624=LINE('',#36140,#7591);
#5625=LINE('',#36145,#7592);
#5626=LINE('',#36147,#7593);
#5627=LINE('',#36149,#7594);
#5628=LINE('',#36150,#7595);
#5629=LINE('',#36153,#7596);
#5630=LINE('',#36155,#7597);
#5631=LINE('',#36157,#7598);
#5632=LINE('',#36159,#7599);
#5633=LINE('',#36160,#7600);
#5634=LINE('',#36164,#7601);
#5635=LINE('',#36165,#7602);
#5636=LINE('',#36167,#7603);
#5637=LINE('',#36168,#7604);
#5638=LINE('',#36172,#7605);
#5639=LINE('',#36174,#7606);
#5640=LINE('',#36175,#7607);
#5641=LINE('',#36177,#7608);
#5642=LINE('',#36178,#7609);
#5643=LINE('',#36181,#7610);
#5644=LINE('',#36183,#7611);
#5645=LINE('',#36184,#7612);
#5646=LINE('',#36185,#7613);
#5647=LINE('',#36188,#7614);
#5648=LINE('',#36189,#7615);
#5649=LINE('',#36193,#7616);
#5650=LINE('',#36194,#7617);
#5651=LINE('',#36196,#7618);
#5652=LINE('',#36199,#7619);
#5653=LINE('',#36200,#7620);
#5654=LINE('',#36202,#7621);
#7588=VECTOR('',#28831,3.);
#7589=VECTOR('',#28838,3.);
#7590=VECTOR('',#28845,4.25000000000001);
#7591=VECTOR('',#28852,4.25000000000001);
#7592=VECTOR('',#28857,1000.);
#7593=VECTOR('',#28858,1000.);
#7594=VECTOR('',#28859,1000.);
#7595=VECTOR('',#28860,1000.);
#7596=VECTOR('',#28863,1000.);
#7597=VECTOR('',#28864,1000.);
#7598=VECTOR('',#28865,1000.);
#7599=VECTOR('',#28866,1000.);
#7600=VECTOR('',#28867,1000.);
#7601=VECTOR('',#28870,1000.);
#7602=VECTOR('',#28871,1000.);
#7603=VECTOR('',#28872,1000.);
#7604=VECTOR('',#28873,1000.);
#7605=VECTOR('',#28876,1000.);
#7606=VECTOR('',#28877,1000.);
#7607=VECTOR('',#28878,1000.);
#7608=VECTOR('',#28879,1000.);
#7609=VECTOR('',#28880,1000.);
#7610=VECTOR('',#28883,1000.);
#7611=VECTOR('',#28884,1000.);
#7612=VECTOR('',#28885,1000.);
#7613=VECTOR('',#28886,1000.);
#7614=VECTOR('',#28889,1000.);
#7615=VECTOR('',#28890,1000.);
#7616=VECTOR('',#28895,1000.);
#7617=VECTOR('',#28896,1000.);
#7618=VECTOR('',#28899,1000.);
#7619=VECTOR('',#28902,1000.);
#7620=VECTOR('',#28903,1000.);
#7621=VECTOR('',#28906,1000.);
#9390=CIRCLE('',#25374,3.);
#9391=CIRCLE('',#25375,3.);
#9392=CIRCLE('',#25377,3.);
#9393=CIRCLE('',#25378,3.);
#9394=CIRCLE('',#25380,4.25000000000001);
#9395=CIRCLE('',#25381,4.25000000000001);
#9396=CIRCLE('',#25383,4.25000000000001);
#9397=CIRCLE('',#25384,4.25000000000001);
#10663=VERTEX_POINT('',#36119);
#10664=VERTEX_POINT('',#36121);
#10665=VERTEX_POINT('',#36125);
#10666=VERTEX_POINT('',#36127);
#10667=VERTEX_POINT('',#36131);
#10668=VERTEX_POINT('',#36133);
#10669=VERTEX_POINT('',#36137);
#10670=VERTEX_POINT('',#36139);
#10671=VERTEX_POINT('',#36143);
#10672=VERTEX_POINT('',#36144);
#10673=VERTEX_POINT('',#36146);
#10674=VERTEX_POINT('',#36148);
#10675=VERTEX_POINT('',#36152);
#10676=VERTEX_POINT('',#36154);
#10677=VERTEX_POINT('',#36156);
#10678=VERTEX_POINT('',#36158);
#10679=VERTEX_POINT('',#36162);
#10680=VERTEX_POINT('',#36163);
#10681=VERTEX_POINT('',#36166);
#10682=VERTEX_POINT('',#36170);
#10683=VERTEX_POINT('',#36171);
#10684=VERTEX_POINT('',#36173);
#10685=VERTEX_POINT('',#36176);
#10686=VERTEX_POINT('',#36180);
#10687=VERTEX_POINT('',#36182);
#10688=VERTEX_POINT('',#36187);
#10689=VERTEX_POINT('',#36192);
#10690=VERTEX_POINT('',#36198);
#13093=EDGE_CURVE('',#10663,#10663,#9390,.T.);
#13094=EDGE_CURVE('',#10663,#10664,#5621,.T.);
#13095=EDGE_CURVE('',#10664,#10664,#9391,.T.);
#13096=EDGE_CURVE('',#10665,#10665,#9392,.T.);
#13097=EDGE_CURVE('',#10665,#10666,#5622,.T.);
#13098=EDGE_CURVE('',#10666,#10666,#9393,.T.);
#13099=EDGE_CURVE('',#10667,#10667,#9394,.T.);
#13100=EDGE_CURVE('',#10667,#10668,#5623,.T.);
#13101=EDGE_CURVE('',#10668,#10668,#9395,.T.);
#13102=EDGE_CURVE('',#10669,#10669,#9396,.T.);
#13103=EDGE_CURVE('',#10669,#10670,#5624,.T.);
#13104=EDGE_CURVE('',#10670,#10670,#9397,.T.);
#13105=EDGE_CURVE('',#10671,#10672,#5625,.T.);
#13106=EDGE_CURVE('',#10673,#10671,#5626,.T.);
#13107=EDGE_CURVE('',#10673,#10674,#5627,.T.);
#13108=EDGE_CURVE('',#10674,#10672,#5628,.T.);
#13109=EDGE_CURVE('',#10675,#10673,#5629,.T.);
#13110=EDGE_CURVE('',#10676,#10675,#5630,.T.);
#13111=EDGE_CURVE('',#10676,#10677,#5631,.T.);
#13112=EDGE_CURVE('',#10677,#10678,#5632,.T.);
#13113=EDGE_CURVE('',#10674,#10678,#5633,.T.);
#13114=EDGE_CURVE('',#10679,#10680,#5634,.T.);
#13115=EDGE_CURVE('',#10679,#10672,#5635,.T.);
#13116=EDGE_CURVE('',#10678,#10681,#5636,.T.);
#13117=EDGE_CURVE('',#10680,#10681,#5637,.T.);
#13118=EDGE_CURVE('',#10682,#10683,#5638,.T.);
#13119=EDGE_CURVE('',#10684,#10682,#5639,.T.);
#13120=EDGE_CURVE('',#10680,#10684,#5640,.T.);
#13121=EDGE_CURVE('',#10681,#10685,#5641,.T.);
#13122=EDGE_CURVE('',#10683,#10685,#5642,.T.);
#13123=EDGE_CURVE('',#10686,#10676,#5643,.T.);
#13124=EDGE_CURVE('',#10686,#10687,#5644,.T.);
#13125=EDGE_CURVE('',#10683,#10687,#5645,.T.);
#13126=EDGE_CURVE('',#10685,#10677,#5646,.T.);
#13127=EDGE_CURVE('',#10688,#10687,#5647,.T.);
#13128=EDGE_CURVE('',#10682,#10688,#5648,.T.);
#13129=EDGE_CURVE('',#10689,#10679,#5649,.T.);
#13130=EDGE_CURVE('',#10689,#10671,#5650,.T.);
#13131=EDGE_CURVE('',#10675,#10689,#5651,.T.);
#13132=EDGE_CURVE('',#10690,#10686,#5652,.T.);
#13133=EDGE_CURVE('',#10690,#10688,#5653,.T.);
#13134=EDGE_CURVE('',#10684,#10690,#5654,.T.);
#17096=ORIENTED_EDGE('',*,*,#13093,.F.);
#17097=ORIENTED_EDGE('',*,*,#13094,.T.);
#17098=ORIENTED_EDGE('',*,*,#13095,.T.);
#17099=ORIENTED_EDGE('',*,*,#13094,.F.);
#17100=ORIENTED_EDGE('',*,*,#13096,.F.);
#17101=ORIENTED_EDGE('',*,*,#13097,.T.);
#17102=ORIENTED_EDGE('',*,*,#13098,.T.);
#17103=ORIENTED_EDGE('',*,*,#13097,.F.);
#17104=ORIENTED_EDGE('',*,*,#13099,.F.);
#17105=ORIENTED_EDGE('',*,*,#13100,.T.);
#17106=ORIENTED_EDGE('',*,*,#13101,.T.);
#17107=ORIENTED_EDGE('',*,*,#13100,.F.);
#17108=ORIENTED_EDGE('',*,*,#13102,.F.);
#17109=ORIENTED_EDGE('',*,*,#13103,.T.);
#17110=ORIENTED_EDGE('',*,*,#13104,.T.);
#17111=ORIENTED_EDGE('',*,*,#13103,.F.);
#17112=ORIENTED_EDGE('',*,*,#13105,.F.);
#17113=ORIENTED_EDGE('',*,*,#13106,.F.);
#17114=ORIENTED_EDGE('',*,*,#13107,.T.);
#17115=ORIENTED_EDGE('',*,*,#13108,.T.);
#17116=ORIENTED_EDGE('',*,*,#13107,.F.);
#17117=ORIENTED_EDGE('',*,*,#13109,.F.);
#17118=ORIENTED_EDGE('',*,*,#13110,.F.);
#17119=ORIENTED_EDGE('',*,*,#13111,.T.);
#17120=ORIENTED_EDGE('',*,*,#13112,.T.);
#17121=ORIENTED_EDGE('',*,*,#13113,.F.);
#17122=ORIENTED_EDGE('',*,*,#13114,.F.);
#17123=ORIENTED_EDGE('',*,*,#13115,.T.);
#17124=ORIENTED_EDGE('',*,*,#13108,.F.);
#17125=ORIENTED_EDGE('',*,*,#13113,.T.);
#17126=ORIENTED_EDGE('',*,*,#13116,.T.);
#17127=ORIENTED_EDGE('',*,*,#13117,.F.);
#17128=ORIENTED_EDGE('',*,*,#13118,.F.);
#17129=ORIENTED_EDGE('',*,*,#13119,.F.);
#17130=ORIENTED_EDGE('',*,*,#13120,.F.);
#17131=ORIENTED_EDGE('',*,*,#13117,.T.);
#17132=ORIENTED_EDGE('',*,*,#13121,.T.);
#17133=ORIENTED_EDGE('',*,*,#13122,.F.);
#17134=ORIENTED_EDGE('',*,*,#13123,.F.);
#17135=ORIENTED_EDGE('',*,*,#13124,.T.);
#17136=ORIENTED_EDGE('',*,*,#13125,.F.);
#17137=ORIENTED_EDGE('',*,*,#13122,.T.);
#17138=ORIENTED_EDGE('',*,*,#13126,.T.);
#17139=ORIENTED_EDGE('',*,*,#13111,.F.);
#17140=ORIENTED_EDGE('',*,*,#13127,.F.);
#17141=ORIENTED_EDGE('',*,*,#13128,.F.);
#17142=ORIENTED_EDGE('',*,*,#13118,.T.);
#17143=ORIENTED_EDGE('',*,*,#13125,.T.);
#17144=ORIENTED_EDGE('',*,*,#13112,.F.);
#17145=ORIENTED_EDGE('',*,*,#13126,.F.);
#17146=ORIENTED_EDGE('',*,*,#13121,.F.);
#17147=ORIENTED_EDGE('',*,*,#13116,.F.);
#17148=ORIENTED_EDGE('',*,*,#13093,.T.);
#17149=ORIENTED_EDGE('',*,*,#13096,.T.);
#17150=ORIENTED_EDGE('',*,*,#13099,.T.);
#17151=ORIENTED_EDGE('',*,*,#13102,.T.);
#17152=ORIENTED_EDGE('',*,*,#13105,.T.);
#17153=ORIENTED_EDGE('',*,*,#13115,.F.);
#17154=ORIENTED_EDGE('',*,*,#13129,.F.);
#17155=ORIENTED_EDGE('',*,*,#13130,.T.);
#17156=ORIENTED_EDGE('',*,*,#13106,.T.);
#17157=ORIENTED_EDGE('',*,*,#13130,.F.);
#17158=ORIENTED_EDGE('',*,*,#13131,.F.);
#17159=ORIENTED_EDGE('',*,*,#13109,.T.);
#17160=ORIENTED_EDGE('',*,*,#13127,.T.);
#17161=ORIENTED_EDGE('',*,*,#13124,.F.);
#17162=ORIENTED_EDGE('',*,*,#13132,.F.);
#17163=ORIENTED_EDGE('',*,*,#13133,.T.);
#17164=ORIENTED_EDGE('',*,*,#13128,.T.);
#17165=ORIENTED_EDGE('',*,*,#13133,.F.);
#17166=ORIENTED_EDGE('',*,*,#13134,.F.);
#17167=ORIENTED_EDGE('',*,*,#13119,.T.);
#17168=ORIENTED_EDGE('',*,*,#13120,.T.);
#17169=ORIENTED_EDGE('',*,*,#13134,.T.);
#17170=ORIENTED_EDGE('',*,*,#13132,.T.);
#17171=ORIENTED_EDGE('',*,*,#13123,.T.);
#17172=ORIENTED_EDGE('',*,*,#13110,.T.);
#17173=ORIENTED_EDGE('',*,*,#13131,.T.);
#17174=ORIENTED_EDGE('',*,*,#13129,.T.);
#17175=ORIENTED_EDGE('',*,*,#13114,.T.);
#17176=ORIENTED_EDGE('',*,*,#13095,.F.);
#17177=ORIENTED_EDGE('',*,*,#13098,.F.);
#17178=ORIENTED_EDGE('',*,*,#13101,.F.);
#17179=ORIENTED_EDGE('',*,*,#13104,.F.);
#22818=CYLINDRICAL_SURFACE('',#25373,3.);
#22819=CYLINDRICAL_SURFACE('',#25376,3.);
#22820=CYLINDRICAL_SURFACE('',#25379,4.25000000000001);
#22821=CYLINDRICAL_SURFACE('',#25382,4.25000000000001);
#23414=ADVANCED_FACE('',(#2422),#22818,.F.);
#23415=ADVANCED_FACE('',(#2423),#22819,.F.);
#23416=ADVANCED_FACE('',(#2424),#22820,.F.);
#23417=ADVANCED_FACE('',(#2425),#22821,.F.);
#23418=ADVANCED_FACE('',(#2426),#1500,.T.);
#23419=ADVANCED_FACE('',(#2427),#1501,.F.);
#23420=ADVANCED_FACE('',(#2428),#1502,.F.);
#23421=ADVANCED_FACE('',(#2429),#1503,.F.);
#23422=ADVANCED_FACE('',(#2430),#1504,.F.);
#23423=ADVANCED_FACE('',(#2431),#1505,.T.);
#23424=ADVANCED_FACE('',(#2432,#1093,#1094,#1095,#1096),#1506,.F.);
#23425=ADVANCED_FACE('',(#2433),#1507,.F.);
#23426=ADVANCED_FACE('',(#2434),#1508,.F.);
#23427=ADVANCED_FACE('',(#2435),#1509,.F.);
#23428=ADVANCED_FACE('',(#2436),#1510,.F.);
#23429=ADVANCED_FACE('',(#2437,#1097,#1098,#1099,#1100),#1511,.T.);
#24536=CLOSED_SHELL('',(#23414,#23415,#23416,#23417,#23418,#23419,#23420,
#23421,#23422,#23423,#23424,#23425,#23426,#23427,#23428,#23429));
#25372=AXIS2_PLACEMENT_3D('',#36117,#28825,#28826);
#25373=AXIS2_PLACEMENT_3D('',#36118,#28827,#28828);
#25374=AXIS2_PLACEMENT_3D('',#36120,#28829,#28830);
#25375=AXIS2_PLACEMENT_3D('',#36123,#28832,#28833);
#25376=AXIS2_PLACEMENT_3D('',#36124,#28834,#28835);
#25377=AXIS2_PLACEMENT_3D('',#36126,#28836,#28837);
#25378=AXIS2_PLACEMENT_3D('',#36129,#28839,#28840);
#25379=AXIS2_PLACEMENT_3D('',#36130,#28841,#28842);
#25380=AXIS2_PLACEMENT_3D('',#36132,#28843,#28844);
#25381=AXIS2_PLACEMENT_3D('',#36135,#28846,#28847);
#25382=AXIS2_PLACEMENT_3D('',#36136,#28848,#28849);
#25383=AXIS2_PLACEMENT_3D('',#36138,#28850,#28851);
#25384=AXIS2_PLACEMENT_3D('',#36141,#28853,#28854);
#25385=AXIS2_PLACEMENT_3D('',#36142,#28855,#28856);
#25386=AXIS2_PLACEMENT_3D('',#36151,#28861,#28862);
#25387=AXIS2_PLACEMENT_3D('',#36161,#28868,#28869);
#25388=AXIS2_PLACEMENT_3D('',#36169,#28874,#28875);
#25389=AXIS2_PLACEMENT_3D('',#36179,#28881,#28882);
#25390=AXIS2_PLACEMENT_3D('',#36186,#28887,#28888);
#25391=AXIS2_PLACEMENT_3D('',#36190,#28891,#28892);
#25392=AXIS2_PLACEMENT_3D('',#36191,#28893,#28894);
#25393=AXIS2_PLACEMENT_3D('',#36195,#28897,#28898);
#25394=AXIS2_PLACEMENT_3D('',#36197,#28900,#28901);
#25395=AXIS2_PLACEMENT_3D('',#36201,#28904,#28905);
#25396=AXIS2_PLACEMENT_3D('',#36203,#28907,#28908);
#28825=DIRECTION('axis',(0.,0.,1.));
#28826=DIRECTION('refdir',(1.,0.,0.));
#28827=DIRECTION('center_axis',(0.,0.,1.));
#28828=DIRECTION('ref_axis',(1.,0.,0.));
#28829=DIRECTION('center_axis',(0.,0.,1.));
#28830=DIRECTION('ref_axis',(1.,0.,0.));
#28831=DIRECTION('',(0.,0.,1.));
#28832=DIRECTION('center_axis',(0.,0.,1.));
#28833=DIRECTION('ref_axis',(1.,0.,0.));
#28834=DIRECTION('center_axis',(0.,0.,1.));
#28835=DIRECTION('ref_axis',(1.,0.,0.));
#28836=DIRECTION('center_axis',(0.,0.,1.));
#28837=DIRECTION('ref_axis',(1.,0.,0.));
#28838=DIRECTION('',(0.,0.,1.));
#28839=DIRECTION('center_axis',(0.,0.,1.));
#28840=DIRECTION('ref_axis',(1.,0.,0.));
#28841=DIRECTION('center_axis',(0.,0.,1.));
#28842=DIRECTION('ref_axis',(1.,0.,0.));
#28843=DIRECTION('center_axis',(0.,0.,1.));
#28844=DIRECTION('ref_axis',(1.,0.,0.));
#28845=DIRECTION('',(0.,0.,1.));
#28846=DIRECTION('center_axis',(0.,0.,1.));
#28847=DIRECTION('ref_axis',(1.,0.,0.));
#28848=DIRECTION('center_axis',(0.,0.,1.));
#28849=DIRECTION('ref_axis',(1.,0.,0.));
#28850=DIRECTION('center_axis',(0.,0.,1.));
#28851=DIRECTION('ref_axis',(1.,0.,0.));
#28852=DIRECTION('',(0.,0.,1.));
#28853=DIRECTION('center_axis',(0.,0.,1.));
#28854=DIRECTION('ref_axis',(1.,0.,0.));
#28855=DIRECTION('center_axis',(0.,0.,1.));
#28856=DIRECTION('ref_axis',(1.,0.,0.));
#28857=DIRECTION('',(-4.08170229641602E-16,1.,0.));
#28858=DIRECTION('',(-1.,0.,0.));
#28859=DIRECTION('',(0.,1.,0.));
#28860=DIRECTION('',(-1.,0.,0.));
#28861=DIRECTION('center_axis',(-1.,0.,0.));
#28862=DIRECTION('ref_axis',(0.,0.,1.));
#28863=DIRECTION('',(0.,0.,1.));
#28864=DIRECTION('',(0.,1.,0.));
#28865=DIRECTION('',(0.,0.,-1.));
#28866=DIRECTION('',(0.,1.,0.));
#28867=DIRECTION('',(0.,0.,-1.));
#28868=DIRECTION('center_axis',(0.,-1.,0.));
#28869=DIRECTION('ref_axis',(0.,0.,-1.));
#28870=DIRECTION('',(-1.,0.,0.));
#28871=DIRECTION('',(0.,0.,1.));
#28872=DIRECTION('',(-1.,0.,0.));
#28873=DIRECTION('',(0.,0.,-1.));
#28874=DIRECTION('center_axis',(1.,0.,0.));
#28875=DIRECTION('ref_axis',(0.,0.,-1.));
#28876=DIRECTION('',(0.,-1.,0.));
#28877=DIRECTION('',(0.,0.,1.));
#28878=DIRECTION('',(0.,-1.,0.));
#28879=DIRECTION('',(0.,-1.,0.));
#28880=DIRECTION('',(0.,0.,-1.));
#28881=DIRECTION('center_axis',(0.,1.,0.));
#28882=DIRECTION('ref_axis',(0.,0.,1.));
#28883=DIRECTION('',(1.,-1.73472347597681E-16,0.));
#28884=DIRECTION('',(0.,0.,1.));
#28885=DIRECTION('',(1.,0.,0.));
#28886=DIRECTION('',(1.,0.,0.));
#28887=DIRECTION('center_axis',(0.,0.,1.));
#28888=DIRECTION('ref_axis',(1.,0.,0.));
#28889=DIRECTION('',(1.73472347597681E-15,-1.,0.));
#28890=DIRECTION('',(1.,0.,0.));
#28891=DIRECTION('center_axis',(0.,0.,1.));
#28892=DIRECTION('ref_axis',(1.,0.,0.));
#28893=DIRECTION('center_axis',(1.,4.08170229641602E-16,0.));
#28894=DIRECTION('ref_axis',(-4.08170229641602E-16,1.,0.));
#28895=DIRECTION('',(-4.08170229641602E-16,1.,0.));
#28896=DIRECTION('',(0.,0.,1.));
#28897=DIRECTION('center_axis',(0.,1.,0.));
#28898=DIRECTION('ref_axis',(0.,0.,1.));
#28899=DIRECTION('',(-1.,0.,0.));
#28900=DIRECTION('center_axis',(-1.,-1.73472347597681E-15,0.));
#28901=DIRECTION('ref_axis',(1.73472347597681E-15,-1.,0.));
#28902=DIRECTION('',(1.73472347597681E-15,-1.,0.));
#28903=DIRECTION('',(0.,0.,1.));
#28904=DIRECTION('center_axis',(0.,-1.,0.));
#28905=DIRECTION('ref_axis',(0.,0.,-1.));
#28906=DIRECTION('',(1.,0.,0.));
#28907=DIRECTION('center_axis',(0.,0.,1.));
#28908=DIRECTION('ref_axis',(1.,0.,0.));
#36117=CARTESIAN_POINT('',(0.,0.,0.));
#36118=CARTESIAN_POINT('Origin',(-13.5,0.5,1.));
#36119=CARTESIAN_POINT('',(-16.5,0.5,-4.));
#36120=CARTESIAN_POINT('Origin',(-13.5,0.5,-4.));
#36121=CARTESIAN_POINT('',(-16.5,0.5,1.));
#36122=CARTESIAN_POINT('',(-16.5,0.5,1.));
#36123=CARTESIAN_POINT('Origin',(-13.5,0.5,1.));
#36124=CARTESIAN_POINT('Origin',(11.5,0.5,1.));
#36125=CARTESIAN_POINT('',(8.5,0.5,-4.));
#36126=CARTESIAN_POINT('Origin',(11.5,0.5,-4.));
#36127=CARTESIAN_POINT('',(8.5,0.5,1.));
#36128=CARTESIAN_POINT('',(8.5,0.5,1.));
#36129=CARTESIAN_POINT('Origin',(11.5,0.5,1.));
#36130=CARTESIAN_POINT('Origin',(-27.,0.5,-4.));
#36131=CARTESIAN_POINT('',(-31.25,0.499999999999999,-4.));
#36132=CARTESIAN_POINT('Origin',(-27.,0.5,-4.));
#36133=CARTESIAN_POINT('',(-31.25,0.499999999999999,1.));
#36134=CARTESIAN_POINT('',(-31.25,0.499999999999999,-4.));
#36135=CARTESIAN_POINT('Origin',(-27.,0.5,1.));
#36136=CARTESIAN_POINT('Origin',(25.,0.5,-4.));
#36137=CARTESIAN_POINT('',(20.75,0.499999999999999,-4.));
#36138=CARTESIAN_POINT('Origin',(25.,0.5,-4.));
#36139=CARTESIAN_POINT('',(20.75,0.499999999999999,1.));
#36140=CARTESIAN_POINT('',(20.75,0.499999999999999,-4.));
#36141=CARTESIAN_POINT('Origin',(25.,0.5,1.));
#36142=CARTESIAN_POINT('Origin',(0.,0.,4.));
#36143=CARTESIAN_POINT('',(34.,-3.5,4.));
#36144=CARTESIAN_POINT('',(34.,13.5,4.));
#36145=CARTESIAN_POINT('',(34.,13.5,4.));
#36146=CARTESIAN_POINT('',(36.5,-3.5,4.));
#36147=CARTESIAN_POINT('',(34.,-3.5,4.));
#36148=CARTESIAN_POINT('',(36.5,13.5,4.));
#36149=CARTESIAN_POINT('',(36.5,13.5,4.));
#36150=CARTESIAN_POINT('',(-36.5,13.5,4.));
#36151=CARTESIAN_POINT('Origin',(36.5,13.5,4.));
#36152=CARTESIAN_POINT('',(36.5,-3.5,1.));
#36153=CARTESIAN_POINT('',(36.5,-3.5,1.));
#36154=CARTESIAN_POINT('',(36.5,-13.5,1.));
#36155=CARTESIAN_POINT('',(36.5,-13.5,1.));
#36156=CARTESIAN_POINT('',(36.5,-13.5,-4.));
#36157=CARTESIAN_POINT('',(36.5,-13.5,4.));
#36158=CARTESIAN_POINT('',(36.5,13.5,-4.));
#36159=CARTESIAN_POINT('',(36.5,13.5,-4.));
#36160=CARTESIAN_POINT('',(36.5,13.5,4.));
#36161=CARTESIAN_POINT('Origin',(-36.5,13.5,4.));
#36162=CARTESIAN_POINT('',(34.,13.5,1.));
#36163=CARTESIAN_POINT('',(-36.5,13.5,1.));
#36164=CARTESIAN_POINT('',(-36.5,13.5,1.));
#36165=CARTESIAN_POINT('',(34.,13.5,1.));
#36166=CARTESIAN_POINT('',(-36.5,13.5,-4.));
#36167=CARTESIAN_POINT('',(-36.5,13.5,-4.));
#36168=CARTESIAN_POINT('',(-36.5,13.5,4.));
#36169=CARTESIAN_POINT('Origin',(-36.5,13.5,4.));
#36170=CARTESIAN_POINT('',(-36.5,-11.5,4.));
#36171=CARTESIAN_POINT('',(-36.5,-13.5,4.));
#36172=CARTESIAN_POINT('',(-36.5,13.5,4.));
#36173=CARTESIAN_POINT('',(-36.5,-11.5,1.));
#36174=CARTESIAN_POINT('',(-36.5,-11.5,1.));
#36175=CARTESIAN_POINT('',(-36.5,13.5,1.));
#36176=CARTESIAN_POINT('',(-36.5,-13.5,-4.));
#36177=CARTESIAN_POINT('',(-36.5,13.5,-4.));
#36178=CARTESIAN_POINT('',(-36.5,-13.5,4.));
#36179=CARTESIAN_POINT('Origin',(-36.5,-13.5,4.));
#36180=CARTESIAN_POINT('',(16.5,-13.5,1.));
#36181=CARTESIAN_POINT('',(16.5,-13.5,1.));
#36182=CARTESIAN_POINT('',(16.5,-13.5,4.));
#36183=CARTESIAN_POINT('',(16.5,-13.5,1.));
#36184=CARTESIAN_POINT('',(-36.5,-13.5,4.));
#36185=CARTESIAN_POINT('',(-36.5,-13.5,-4.));
#36186=CARTESIAN_POINT('Origin',(0.,0.,4.));
#36187=CARTESIAN_POINT('',(16.5,-11.5,4.));
#36188=CARTESIAN_POINT('',(16.5,-11.5,4.));
#36189=CARTESIAN_POINT('',(-36.5,-11.5,4.));
#36190=CARTESIAN_POINT('Origin',(0.,0.,-4.));
#36191=CARTESIAN_POINT('Origin',(34.,13.5,1.));
#36192=CARTESIAN_POINT('',(34.,-3.5,1.));
#36193=CARTESIAN_POINT('',(34.,13.5,1.));
#36194=CARTESIAN_POINT('',(34.,-3.5,1.));
#36195=CARTESIAN_POINT('Origin',(34.,-3.5,1.));
#36196=CARTESIAN_POINT('',(34.,-3.5,1.));
#36197=CARTESIAN_POINT('Origin',(16.5,-11.5,1.));
#36198=CARTESIAN_POINT('',(16.5,-11.5,1.));
#36199=CARTESIAN_POINT('',(16.5,-11.5,1.));
#36200=CARTESIAN_POINT('',(16.5,-11.5,1.));
#36201=CARTESIAN_POINT('Origin',(-36.5,-11.5,1.));
#36202=CARTESIAN_POINT('',(-36.5,-11.5,1.));
#36203=CARTESIAN_POINT('Origin',(0.,0.,1.));
#57015=UNCERTAINTY_MEASURE_WITH_UNIT(LENGTH_MEASURE(0.01),#57080,
'DISTANCE_ACCURACY_VALUE',
'Maximum model space distance between geometric entities at asserted c
onnectivities');
#57040=UNCERTAINTY_MEASURE_WITH_UNIT(LENGTH_MEASURE(0.01),#57080,
'DISTANCE_ACCURACY_VALUE',
'Maximum model space distance between geometric entities at asserted c
onnectivities');
#57054=(
GEOMETRIC_REPRESENTATION_CONTEXT(3)
GLOBAL_UNCERTAINTY_ASSIGNED_CONTEXT((#57015))
GLOBAL_UNIT_ASSIGNED_CONTEXT((#57080,#57082,#57083))
REPRESENTATION_CONTEXT('','3D')
);
#57079=(
GEOMETRIC_REPRESENTATION_CONTEXT(3)
GLOBAL_UNCERTAINTY_ASSIGNED_CONTEXT((#57040))
GLOBAL_UNIT_ASSIGNED_CONTEXT((#57080,#57082,#57083))
REPRESENTATION_CONTEXT('','3D')
);
#57080=(
LENGTH_UNIT()
NAMED_UNIT(*)
SI_UNIT(.MILLI.,.METRE.)
);
#57082=(
NAMED_UNIT(*)
PLANE_ANGLE_UNIT()
SI_UNIT($,.RADIAN.)
);
#57083=(
NAMED_UNIT(*)
SI_UNIT($,.STERADIAN.)
SOLID_ANGLE_UNIT()
);
#57097=SHAPE_DEFINITION_REPRESENTATION(#57143,#57262);
#57143=PRODUCT_DEFINITION_SHAPE('',$,#57301);
#57262=SHAPE_REPRESENTATION('',(#25372),#57054);
#57287=PRODUCT_DEFINITION_CONTEXT('part definition',#57403,'design');
#57301=PRODUCT_DEFINITION('Ball Screw Spacer 1','Ball Screw Spacer 1',#57339,
#57287);
#57339=PRODUCT_DEFINITION_FORMATION('',$,#57418);
#57403=APPLICATION_CONTEXT(
'Core Data for Automotive Mechanical Design Process');
#57404=PRODUCT_CONTEXT('part definition',#57403,'mechanical');
#57418=PRODUCT('Ball Screw Spacer 1','Ball Screw Spacer 1',$,(#57404));
#57444=PRESENTATION_STYLE_ASSIGNMENT((#57446));
#57446=SURFACE_STYLE_USAGE(.BOTH.,#57448);
#57448=SURFACE_SIDE_STYLE('',(#57450));
#57450=SURFACE_STYLE_FILL_AREA(#57452);
#57452=FILL_AREA_STYLE('Opaque(202,209,238)',(#57454));
#57454=FILL_AREA_STYLE_COLOUR('Opaque(202,209,238)',#57456);
#57456=COLOUR_RGB('Opaque(202,209,238)',0.792156862745098,0.819607843137255,
0.933333333333333);
ENDSEC;
END-ISO-10303-21;
